ISO-10303-21;
HEADER;
/* Generated by software containing ST-Developer
 * from STEP Tools, Inc. (www.steptools.com) 
 */

FILE_DESCRIPTION(
/* description */ (''),
/* implementation_level */ '2;1');

FILE_NAME(
/* name */ 'Hex Bolt - M8x40.step',
/* time_stamp */ '2026-10-29T16:43:51-07:00',
/* author */ (''),
/* organization */ (''),
/* preprocessor_version */ 'ST-DEVELOPER v20.2',
/* originating_system */ 'Autodesk Translation Framework v15.17.0.0',
/* authorisation */ '');

FILE_SCHEMA (('AUTOMOTIVE_DESIGN { 1 0 10303 214 3 1 1 }'));
ENDSEC;

DATA;
#10=MECHANICAL_DESIGN_GEOMETRIC_PRESENTATION_REPRESENTATION('',(#373),#10292);
#265=(
BOUNDED_CURVE()
B_SPLINE_CURVE(2,(#7989,#7990,#7991),.UNSPECIFIED.,.F.,.F.)
B_SPLINE_CURVE_WITH_KNOTS((3,3),(0.14973948338295,0.97160236658079),
 .UNSPECIFIED.)
CURVE()
GEOMETRIC_REPRESENTATION_ITEM()
RATIONAL_B_SPLINE_CURVE((1.07140024848292,1.23714644374248,1.07140024848292))
REPRESENTATION_ITEM('')
);
#266=(
BOUNDED_CURVE()
B_SPLINE_CURVE(2,(#7993,#7994,#7995),.UNSPECIFIED.,.F.,.F.)
B_SPLINE_CURVE_WITH_KNOTS((3,3),(0.14973948338295,0.97160236658079),
 .UNSPECIFIED.)
CURVE()
GEOMETRIC_REPRESENTATION_ITEM()
RATIONAL_B_SPLINE_CURVE((1.07140024848292,1.23714644374248,1.07140024848292))
REPRESENTATION_ITEM('')
);
#267=(
BOUNDED_CURVE()
B_SPLINE_CURVE(2,(#7997,#7998,#7999),.UNSPECIFIED.,.F.,.F.)
B_SPLINE_CURVE_WITH_KNOTS((3,3),(0.14973948338295,0.97160236658079),
 .UNSPECIFIED.)
CURVE()
GEOMETRIC_REPRESENTATION_ITEM()
RATIONAL_B_SPLINE_CURVE((1.07140024848292,1.23714644374248,1.07140024848292))
REPRESENTATION_ITEM('')
);
#268=(
BOUNDED_CURVE()
B_SPLINE_CURVE(2,(#8001,#8002,#8003),.UNSPECIFIED.,.F.,.F.)
B_SPLINE_CURVE_WITH_KNOTS((3,3),(0.149739483382949,0.971602366580789),
 .UNSPECIFIED.)
CURVE()
GEOMETRIC_REPRESENTATION_ITEM()
RATIONAL_B_SPLINE_CURVE((1.07140024848292,1.23714644374248,1.07140024848292))
REPRESENTATION_ITEM('')
);
#269=(
BOUNDED_CURVE()
B_SPLINE_CURVE(2,(#8005,#8006,#8007),.UNSPECIFIED.,.F.,.F.)
B_SPLINE_CURVE_WITH_KNOTS((3,3),(0.14973948338295,0.971602366580789),
 .UNSPECIFIED.)
CURVE()
GEOMETRIC_REPRESENTATION_ITEM()
RATIONAL_B_SPLINE_CURVE((1.07140024848292,1.23714644374248,1.07140024848292))
REPRESENTATION_ITEM('')
);
#270=(
BOUNDED_CURVE()
B_SPLINE_CURVE(2,(#8008,#8009,#8010),.UNSPECIFIED.,.F.,.F.)
B_SPLINE_CURVE_WITH_KNOTS((3,3),(0.14973948338295,0.97160236658079),
 .UNSPECIFIED.)
CURVE()
GEOMETRIC_REPRESENTATION_ITEM()
RATIONAL_B_SPLINE_CURVE((1.07140024848292,1.23714644374248,1.07140024848292))
REPRESENTATION_ITEM('')
);
#301=CONICAL_SURFACE('',#5501,0.36,0.785398163397451);
#302=CONICAL_SURFACE('',#5504,0.734027674973257,1.0471975511966);
#327=SHAPE_REPRESENTATION_RELATIONSHIP('SRR','None',#10423,#350);
#350=ADVANCED_BREP_SHAPE_REPRESENTATION('',(#394),#10275);
#373=STYLED_ITEM('',(#10635),#394);
#394=MANIFOLD_SOLID_BREP('Body1',#5017);
#467=FACE_BOUND('',#1187,.T.);
#602=PLANE('',#5503);
#603=PLANE('',#5506);
#604=PLANE('',#5507);
#605=PLANE('',#5508);
#606=PLANE('',#5509);
#607=PLANE('',#5510);
#608=PLANE('',#5511);
#609=PLANE('',#5512);
#610=PLANE('',#5513);
#826=FACE_OUTER_BOUND('',#1175,.T.);
#827=FACE_OUTER_BOUND('',#1176,.T.);
#828=FACE_OUTER_BOUND('',#1177,.T.);
#829=FACE_OUTER_BOUND('',#1178,.T.);
#830=FACE_OUTER_BOUND('',#1179,.T.);
#831=FACE_OUTER_BOUND('',#1180,.T.);
#832=FACE_OUTER_BOUND('',#1181,.T.);
#833=FACE_OUTER_BOUND('',#1182,.T.);
#834=FACE_OUTER_BOUND('',#1183,.T.);
#835=FACE_OUTER_BOUND('',#1184,.T.);
#836=FACE_OUTER_BOUND('',#1185,.T.);
#837=FACE_OUTER_BOUND('',#1186,.T.);
#1175=EDGE_LOOP('',(#3939,#3940,#3941,#3942));
#1176=EDGE_LOOP('',(#3943,#3944,#3945,#3946));
#1177=EDGE_LOOP('',(#3947));
#1178=EDGE_LOOP('',(#3948,#3949,#3950,#3951,#3952,#3953,#3954,#3955,#3956));
#1179=EDGE_LOOP('',(#3957,#3958,#3959,#3960));
#1180=EDGE_LOOP('',(#3961,#3962,#3963,#3964));
#1181=EDGE_LOOP('',(#3965,#3966,#3967,#3968));
#1182=EDGE_LOOP('',(#3969,#3970,#3971,#3972));
#1183=EDGE_LOOP('',(#3973,#3974,#3975,#3976));
#1184=EDGE_LOOP('',(#3977,#3978,#3979,#3980));
#1185=EDGE_LOOP('',(#3981));
#1186=EDGE_LOOP('',(#3982,#3983,#3984,#3985,#3986,#3987));
#1187=EDGE_LOOP('',(#3988));
#1594=LINE('',#7976,#1986);
#1595=LINE('',#7981,#1987);
#1596=LINE('',#7987,#1988);
#1597=LINE('',#8013,#1989);
#1598=LINE('',#8015,#1990);
#1599=LINE('',#8016,#1991);
#1600=LINE('',#8019,#1992);
#1601=LINE('',#8020,#1993);
#1602=LINE('',#8023,#1994);
#1603=LINE('',#8024,#1995);
#1604=LINE('',#8027,#1996);
#1605=LINE('',#8028,#1997);
#1606=LINE('',#8031,#1998);
#1607=LINE('',#8032,#1999);
#1608=LINE('',#8034,#2000);
#1986=VECTOR('',#6469,0.4);
#1987=VECTOR('',#6476,0.36);
#1988=VECTOR('',#6483,0.734027674973257);
#1989=VECTOR('',#6486,1.);
#1990=VECTOR('',#6487,1.);
#1991=VECTOR('',#6488,1.);
#1992=VECTOR('',#6491,1.);
#1993=VECTOR('',#6492,1.);
#1994=VECTOR('',#6495,1.);
#1995=VECTOR('',#6496,1.);
#1996=VECTOR('',#6499,1.);
#1997=VECTOR('',#6500,1.);
#1998=VECTOR('',#6503,1.);
#1999=VECTOR('',#6504,1.);
#2000=VECTOR('',#6507,1.);
#2277=CIRCLE('',#5499,0.3933);
#2278=CIRCLE('',#5500,0.3933);
#2279=CIRCLE('',#5502,0.32);
#2280=CIRCLE('',#5505,0.6175);
#2568=VERTEX_POINT('',#7973);
#2569=VERTEX_POINT('',#7975);
#2570=VERTEX_POINT('',#7979);
#2571=VERTEX_POINT('',#7984);
#2572=VERTEX_POINT('',#7986);
#2573=VERTEX_POINT('',#7988);
#2574=VERTEX_POINT('',#7992);
#2575=VERTEX_POINT('',#7996);
#2576=VERTEX_POINT('',#8000);
#2577=VERTEX_POINT('',#8004);
#2578=VERTEX_POINT('',#8012);
#2579=VERTEX_POINT('',#8014);
#2580=VERTEX_POINT('',#8018);
#2581=VERTEX_POINT('',#8022);
#2582=VERTEX_POINT('',#8026);
#2583=VERTEX_POINT('',#8030);
#3060=EDGE_CURVE('',#2568,#2568,#2277,.F.);
#3061=EDGE_CURVE('',#2568,#2569,#1594,.T.);
#3062=EDGE_CURVE('',#2569,#2569,#2278,.F.);
#3063=EDGE_CURVE('',#2570,#2570,#2279,.T.);
#3064=EDGE_CURVE('',#2570,#2568,#1595,.T.);
#3065=EDGE_CURVE('',#2571,#2571,#2280,.T.);
#3066=EDGE_CURVE('',#2571,#2572,#1596,.T.);
#3067=EDGE_CURVE('',#2573,#2572,#265,.T.);
#3068=EDGE_CURVE('',#2574,#2573,#266,.T.);
#3069=EDGE_CURVE('',#2575,#2574,#267,.T.);
#3070=EDGE_CURVE('',#2576,#2575,#268,.T.);
#3071=EDGE_CURVE('',#2577,#2576,#269,.T.);
#3072=EDGE_CURVE('',#2572,#2577,#270,.T.);
#3073=EDGE_CURVE('',#2578,#2576,#1597,.T.);
#3074=EDGE_CURVE('',#2578,#2579,#1598,.T.);
#3075=EDGE_CURVE('',#2579,#2577,#1599,.T.);
#3076=EDGE_CURVE('',#2580,#2575,#1600,.T.);
#3077=EDGE_CURVE('',#2580,#2578,#1601,.T.);
#3078=EDGE_CURVE('',#2581,#2574,#1602,.T.);
#3079=EDGE_CURVE('',#2581,#2580,#1603,.T.);
#3080=EDGE_CURVE('',#2582,#2573,#1604,.T.);
#3081=EDGE_CURVE('',#2582,#2581,#1605,.T.);
#3082=EDGE_CURVE('',#2583,#2572,#1606,.T.);
#3083=EDGE_CURVE('',#2583,#2582,#1607,.T.);
#3084=EDGE_CURVE('',#2579,#2583,#1608,.T.);
#3939=ORIENTED_EDGE('',*,*,#3060,.F.);
#3940=ORIENTED_EDGE('',*,*,#3061,.T.);
#3941=ORIENTED_EDGE('',*,*,#3062,.F.);
#3942=ORIENTED_EDGE('',*,*,#3061,.F.);
#3943=ORIENTED_EDGE('',*,*,#3063,.F.);
#3944=ORIENTED_EDGE('',*,*,#3064,.T.);
#3945=ORIENTED_EDGE('',*,*,#3060,.T.);
#3946=ORIENTED_EDGE('',*,*,#3064,.F.);
#3947=ORIENTED_EDGE('',*,*,#3063,.T.);
#3948=ORIENTED_EDGE('',*,*,#3065,.F.);
#3949=ORIENTED_EDGE('',*,*,#3066,.T.);
#3950=ORIENTED_EDGE('',*,*,#3067,.F.);
#3951=ORIENTED_EDGE('',*,*,#3068,.F.);
#3952=ORIENTED_EDGE('',*,*,#3069,.F.);
#3953=ORIENTED_EDGE('',*,*,#3070,.F.);
#3954=ORIENTED_EDGE('',*,*,#3071,.F.);
#3955=ORIENTED_EDGE('',*,*,#3072,.F.);
#3956=ORIENTED_EDGE('',*,*,#3066,.F.);
#3957=ORIENTED_EDGE('',*,*,#3071,.T.);
#3958=ORIENTED_EDGE('',*,*,#3073,.F.);
#3959=ORIENTED_EDGE('',*,*,#3074,.T.);
#3960=ORIENTED_EDGE('',*,*,#3075,.T.);
#3961=ORIENTED_EDGE('',*,*,#3070,.T.);
#3962=ORIENTED_EDGE('',*,*,#3076,.F.);
#3963=ORIENTED_EDGE('',*,*,#3077,.T.);
#3964=ORIENTED_EDGE('',*,*,#3073,.T.);
#3965=ORIENTED_EDGE('',*,*,#3069,.T.);
#3966=ORIENTED_EDGE('',*,*,#3078,.F.);
#3967=ORIENTED_EDGE('',*,*,#3079,.T.);
#3968=ORIENTED_EDGE('',*,*,#3076,.T.);
#3969=ORIENTED_EDGE('',*,*,#3068,.T.);
#3970=ORIENTED_EDGE('',*,*,#3080,.F.);
#3971=ORIENTED_EDGE('',*,*,#3081,.T.);
#3972=ORIENTED_EDGE('',*,*,#3078,.T.);
#3973=ORIENTED_EDGE('',*,*,#3067,.T.);
#3974=ORIENTED_EDGE('',*,*,#3082,.F.);
#3975=ORIENTED_EDGE('',*,*,#3083,.T.);
#3976=ORIENTED_EDGE('',*,*,#3080,.T.);
#3977=ORIENTED_EDGE('',*,*,#3072,.T.);
#3978=ORIENTED_EDGE('',*,*,#3075,.F.);
#3979=ORIENTED_EDGE('',*,*,#3084,.T.);
#3980=ORIENTED_EDGE('',*,*,#3082,.T.);
#3981=ORIENTED_EDGE('',*,*,#3065,.T.);
#3982=ORIENTED_EDGE('',*,*,#3079,.F.);
#3983=ORIENTED_EDGE('',*,*,#3081,.F.);
#3984=ORIENTED_EDGE('',*,*,#3083,.F.);
#3985=ORIENTED_EDGE('',*,*,#3084,.F.);
#3986=ORIENTED_EDGE('',*,*,#3074,.F.);
#3987=ORIENTED_EDGE('',*,*,#3077,.F.);
#3988=ORIENTED_EDGE('',*,*,#3062,.T.);
#4674=CYLINDRICAL_SURFACE('',#5498,0.3933);
#4835=ADVANCED_FACE('',(#826),#4674,.T.);
#4836=ADVANCED_FACE('',(#827),#301,.T.);
#4837=ADVANCED_FACE('',(#828),#602,.T.);
#4838=ADVANCED_FACE('',(#829),#302,.T.);
#4839=ADVANCED_FACE('',(#830),#603,.T.);
#4840=ADVANCED_FACE('',(#831),#604,.T.);
#4841=ADVANCED_FACE('',(#832),#605,.T.);
#4842=ADVANCED_FACE('',(#833),#606,.T.);
#4843=ADVANCED_FACE('',(#834),#607,.T.);
#4844=ADVANCED_FACE('',(#835),#608,.T.);
#4845=ADVANCED_FACE('',(#836),#609,.T.);
#4846=ADVANCED_FACE('',(#837,#467),#610,.F.);
#5017=CLOSED_SHELL('',(#4835,#4836,#4837,#4838,#4839,#4840,#4841,#4842,
#4843,#4844,#4845,#4846));
#5497=AXIS2_PLACEMENT_3D('',#7971,#6463,#6464);
#5498=AXIS2_PLACEMENT_3D('',#7972,#6465,#6466);
#5499=AXIS2_PLACEMENT_3D('',#7974,#6467,#6468);
#5500=AXIS2_PLACEMENT_3D('',#7977,#6470,#6471);
#5501=AXIS2_PLACEMENT_3D('',#7978,#6472,#6473);
#5502=AXIS2_PLACEMENT_3D('',#7980,#6474,#6475);
#5503=AXIS2_PLACEMENT_3D('',#7982,#6477,#6478);
#5504=AXIS2_PLACEMENT_3D('',#7983,#6479,#6480);
#5505=AXIS2_PLACEMENT_3D('',#7985,#6481,#6482);
#5506=AXIS2_PLACEMENT_3D('',#8011,#6484,#6485);
#5507=AXIS2_PLACEMENT_3D('',#8017,#6489,#6490);
#5508=AXIS2_PLACEMENT_3D('',#8021,#6493,#6494);
#5509=AXIS2_PLACEMENT_3D('',#8025,#6497,#6498);
#5510=AXIS2_PLACEMENT_3D('',#8029,#6501,#6502);
#5511=AXIS2_PLACEMENT_3D('',#8033,#6505,#6506);
#5512=AXIS2_PLACEMENT_3D('',#8035,#6508,#6509);
#5513=AXIS2_PLACEMENT_3D('',#8036,#6510,#6511);
#6463=DIRECTION('axis',(0.,0.,1.));
#6464=DIRECTION('refdir',(1.,0.,0.));
#6465=DIRECTION('center_axis',(0.,-1.,0.));
#6466=DIRECTION('ref_axis',(1.,0.,0.));
#6467=DIRECTION('center_axis',(0.,1.,0.));
#6468=DIRECTION('ref_axis',(1.,0.,0.));
#6469=DIRECTION('',(0.,1.,0.));
#6470=DIRECTION('center_axis',(0.,-1.,0.));
#6471=DIRECTION('ref_axis',(1.,0.,0.));
#6472=DIRECTION('center_axis',(0.,1.,0.));
#6473=DIRECTION('ref_axis',(1.,0.,0.));
#6474=DIRECTION('center_axis',(0.,-1.,0.));
#6475=DIRECTION('ref_axis',(1.,0.,0.));
#6476=DIRECTION('',(-0.707106781186549,0.707106781186546,-8.65956056235496E-17));
#6477=DIRECTION('center_axis',(0.,-1.,0.));
#6478=DIRECTION('ref_axis',(0.,0.,-1.));
#6479=DIRECTION('center_axis',(0.,-1.,0.));
#6480=DIRECTION('ref_axis',(1.,0.,0.));
#6481=DIRECTION('center_axis',(0.,1.,0.));
#6482=DIRECTION('ref_axis',(1.,0.,0.));
#6483=DIRECTION('',(-0.866025403784439,-0.5,-1.06057523872491E-16));
#6484=DIRECTION('center_axis',(1.4792020664489E-16,0.,-1.));
#6485=DIRECTION('ref_axis',(-1.,0.,-1.4792020664489E-16));
#6486=DIRECTION('',(0.,1.,0.));
#6487=DIRECTION('',(-1.,0.,-1.4792020664489E-16));
#6488=DIRECTION('',(0.,1.,0.));
#6489=DIRECTION('center_axis',(0.866025403784439,0.,-0.5));
#6490=DIRECTION('ref_axis',(-0.5,0.,-0.866025403784439));
#6491=DIRECTION('',(0.,1.,0.));
#6492=DIRECTION('',(-0.5,0.,-0.866025403784439));
#6493=DIRECTION('center_axis',(0.866025403784439,0.,0.5));
#6494=DIRECTION('ref_axis',(0.5,0.,-0.866025403784439));
#6495=DIRECTION('',(0.,1.,0.));
#6496=DIRECTION('',(0.5,0.,-0.866025403784439));
#6497=DIRECTION('center_axis',(-2.95840413289779E-16,0.,1.));
#6498=DIRECTION('ref_axis',(1.,0.,2.95840413289779E-16));
#6499=DIRECTION('',(0.,1.,0.));
#6500=DIRECTION('',(1.,0.,2.95840413289779E-16));
#6501=DIRECTION('center_axis',(-0.866025403784439,0.,0.5));
#6502=DIRECTION('ref_axis',(0.5,0.,0.866025403784439));
#6503=DIRECTION('',(0.,1.,0.));
#6504=DIRECTION('',(0.5,0.,0.866025403784439));
#6505=DIRECTION('center_axis',(-0.866025403784439,0.,-0.5));
#6506=DIRECTION('ref_axis',(-0.5,0.,0.866025403784439));
#6507=DIRECTION('',(-0.5,0.,0.866025403784439));
#6508=DIRECTION('center_axis',(0.,1.,0.));
#6509=DIRECTION('ref_axis',(0.,0.,1.));
#6510=DIRECTION('center_axis',(0.,1.,0.));
#6511=DIRECTION('ref_axis',(1.,0.,0.));
#7971=CARTESIAN_POINT('',(0.,0.,0.));
#7972=CARTESIAN_POINT('Origin',(0.,-1.935,0.));
#7973=CARTESIAN_POINT('',(-0.3933,-3.9267,4.81653586104654E-17));
#7974=CARTESIAN_POINT('Origin',(0.,-3.9267,0.));
#7975=CARTESIAN_POINT('',(-0.3933,0.,-4.81653586104654E-17));
#7976=CARTESIAN_POINT('',(-0.3933,-1.935,-4.81653586104654E-17));
#7977=CARTESIAN_POINT('Origin',(0.,0.,0.));
#7978=CARTESIAN_POINT('Origin',(0.,-3.96,0.));
#7979=CARTESIAN_POINT('',(-0.32,-4.,-3.91886975727153E-17));
#7980=CARTESIAN_POINT('Origin',(0.,-4.,0.));
#7981=CARTESIAN_POINT('',(-0.36,-3.96,-4.40872847693047E-17));
#7982=CARTESIAN_POINT('Origin',(0.,-4.,0.));
#7983=CARTESIAN_POINT('Origin',(0.,0.462722715486149,0.));
#7984=CARTESIAN_POINT('',(-0.6175,0.53,-7.5621939847349E-17));
#7985=CARTESIAN_POINT('Origin',(0.,0.53,0.));
#7986=CARTESIAN_POINT('',(-0.750555349946514,0.453180457891261,-9.19165206894919E-17));
#7987=CARTESIAN_POINT('',(-0.734027674973257,0.462722715486149,-8.98924642641573E-17));
#7988=CARTESIAN_POINT('',(-0.375277674973257,0.453180457891261,0.65));
#7989=CARTESIAN_POINT('Ctrl Pts',(-0.375277674973257,0.45318045789126,0.65));
#7990=CARTESIAN_POINT('Ctrl Pts',(-0.562916512459968,0.561513791224244,
0.324999999999856));
#7991=CARTESIAN_POINT('Ctrl Pts',(-0.750555349946514,0.45318045789126,-9.19165206894919E-17));
#7992=CARTESIAN_POINT('',(0.375277674973257,0.453180457891261,0.65));
#7993=CARTESIAN_POINT('Ctrl Pts',(0.375277674973257,0.453180457891261,0.65));
#7994=CARTESIAN_POINT('Ctrl Pts',(-1.66922031752392E-13,0.561513791224244,
0.65));
#7995=CARTESIAN_POINT('Ctrl Pts',(-0.375277674973257,0.45318045789126,0.65));
#7996=CARTESIAN_POINT('',(0.750555349946514,0.453180457891261,0.));
#7997=CARTESIAN_POINT('Ctrl Pts',(0.750555349946514,0.453180457891261,0.));
#7998=CARTESIAN_POINT('Ctrl Pts',(0.562916512459802,0.561513791224244,0.325000000000144));
#7999=CARTESIAN_POINT('Ctrl Pts',(0.375277674973257,0.45318045789126,0.65));
#8000=CARTESIAN_POINT('',(0.375277674973257,0.453180457891261,-0.65));
#8001=CARTESIAN_POINT('Ctrl Pts',(0.375277674973257,0.45318045789126,-0.65));
#8002=CARTESIAN_POINT('Ctrl Pts',(0.562916512459968,0.561513791224244,-0.324999999999855));
#8003=CARTESIAN_POINT('Ctrl Pts',(0.750555349946514,0.453180457891261,0.));
#8004=CARTESIAN_POINT('',(-0.375277674973257,0.45318045789126,-0.65));
#8005=CARTESIAN_POINT('Ctrl Pts',(-0.375277674973257,0.453180457891261,
-0.65));
#8006=CARTESIAN_POINT('Ctrl Pts',(1.66866520601161E-13,0.561513791224244,
-0.65));
#8007=CARTESIAN_POINT('Ctrl Pts',(0.375277674973257,0.45318045789126,-0.65));
#8008=CARTESIAN_POINT('Ctrl Pts',(-0.750555349946514,0.453180457891261,
-9.19165206894919E-17));
#8009=CARTESIAN_POINT('Ctrl Pts',(-0.562916512459802,0.561513791224244,
-0.325000000000144));
#8010=CARTESIAN_POINT('Ctrl Pts',(-0.375277674973257,0.45318045789126,-0.65));
#8011=CARTESIAN_POINT('Origin',(0.375277674973257,0.,-0.65));
#8012=CARTESIAN_POINT('',(0.375277674973257,0.,-0.65));
#8013=CARTESIAN_POINT('',(0.375277674973257,0.,-0.65));
#8014=CARTESIAN_POINT('',(-0.375277674973257,0.,-0.65));
#8015=CARTESIAN_POINT('',(0.375277674973257,0.,-0.65));
#8016=CARTESIAN_POINT('',(-0.375277674973257,0.,-0.65));
#8017=CARTESIAN_POINT('Origin',(0.750555349946514,0.,0.));
#8018=CARTESIAN_POINT('',(0.750555349946514,0.,0.));
#8019=CARTESIAN_POINT('',(0.750555349946514,0.,0.));
#8020=CARTESIAN_POINT('',(0.750555349946514,0.,0.));
#8021=CARTESIAN_POINT('Origin',(0.375277674973257,0.,0.65));
#8022=CARTESIAN_POINT('',(0.375277674973257,0.,0.65));
#8023=CARTESIAN_POINT('',(0.375277674973257,0.,0.65));
#8024=CARTESIAN_POINT('',(0.375277674973257,0.,0.65));
#8025=CARTESIAN_POINT('Origin',(-0.375277674973257,0.,0.65));
#8026=CARTESIAN_POINT('',(-0.375277674973257,0.,0.65));
#8027=CARTESIAN_POINT('',(-0.375277674973257,0.,0.65));
#8028=CARTESIAN_POINT('',(-0.375277674973257,0.,0.65));
#8029=CARTESIAN_POINT('Origin',(-0.750555349946514,0.,-9.19165206894919E-17));
#8030=CARTESIAN_POINT('',(-0.750555349946514,0.,-9.19165206894919E-17));
#8031=CARTESIAN_POINT('',(-0.750555349946514,0.,-9.19165206894919E-17));
#8032=CARTESIAN_POINT('',(-0.750555349946514,0.,-9.19165206894919E-17));
#8033=CARTESIAN_POINT('Origin',(-0.375277674973257,0.,-0.65));
#8034=CARTESIAN_POINT('',(-0.375277674973257,0.,-0.65));
#8035=CARTESIAN_POINT('Origin',(0.,0.53,-1.11022302462516E-16));
#8036=CARTESIAN_POINT('Origin',(0.,0.,-1.11022302462516E-16));
#10247=UNCERTAINTY_MEASURE_WITH_UNIT(LENGTH_MEASURE(0.001),#10293,
'DISTANCE_ACCURACY_VALUE',
'Maximum model space distance between geometric entities at asserted c
onnectivities');
#10264=UNCERTAINTY_MEASURE_WITH_UNIT(LENGTH_MEASURE(0.001),#10293,
'DISTANCE_ACCURACY_VALUE',
'Maximum model space distance between geometric entities at asserted c
onnectivities');
#10275=(
GEOMETRIC_REPRESENTATION_CONTEXT(3)
GLOBAL_UNCERTAINTY_ASSIGNED_CONTEXT((#10247))
GLOBAL_UNIT_ASSIGNED_CONTEXT((#10293,#10295,#10296))
REPRESENTATION_CONTEXT('','3D')
);
#10292=(
GEOMETRIC_REPRESENTATION_CONTEXT(3)
GLOBAL_UNCERTAINTY_ASSIGNED_CONTEXT((#10264))
GLOBAL_UNIT_ASSIGNED_CONTEXT((#10293,#10295,#10296))
REPRESENTATION_CONTEXT('','3D')
);
#10293=(
LENGTH_UNIT()
NAMED_UNIT(*)
SI_UNIT(.CENTI.,.METRE.)
);
#10295=(
NAMED_UNIT(*)
PLANE_ANGLE_UNIT()
SI_UNIT($,.RADIAN.)
);
#10296=(
NAMED_UNIT(*)
SI_UNIT($,.STERADIAN.)
SOLID_ANGLE_UNIT()
);
#10307=SHAPE_DEFINITION_REPRESENTATION(#10334,#10423);
#10334=PRODUCT_DEFINITION_SHAPE('',$,#10451);
#10423=SHAPE_REPRESENTATION('',(#5497),#10275);
#10440=PRODUCT_DEFINITION_CONTEXT('part definition',#10523,'design');
#10451=PRODUCT_DEFINITION('Hex Bolt - M8x40','Hex Bolt - M8x40',
#10478,#10440);
#10478=PRODUCT_DEFINITION_FORMATION('',$,#10535);
#10523=APPLICATION_CONTEXT(
'Core Data for Automotive Mechanical Design Process');
#10524=PRODUCT_CONTEXT('part definition',#10523,'mechanical');
#10535=PRODUCT('Hex Bolt - M8x40','Hex Bolt - M8x40',
'Hex Bolt - M8x40',(#10524));
#10629=COLOUR_RGB('Black',0.12,0.14,0.17);
#10630=FILL_AREA_STYLE_COLOUR('',#10629);
#10631=FILL_AREA_STYLE('',(#10630));
#10632=SURFACE_STYLE_FILL_AREA(#10631);
#10633=SURFACE_SIDE_STYLE('',(#10632));
#10634=SURFACE_STYLE_USAGE(.BOTH.,#10633);
#10635=PRESENTATION_STYLE_ASSIGNMENT((#10634));
ENDSEC;
END-ISO-10303-21;
